ISO-10303-21;
HEADER;
/* Generated by software containing ST-Developer
 * from STEP Tools, Inc. (www.steptools.com) 
 */

FILE_DESCRIPTION(
/* description */ ('Flywheel Crank-Slider'),
/* implementation_level */ '2;1');

FILE_NAME(
/* name */ 'Bearing bolt reducer (3).step',
/* time_stamp */ '2026-10-28T03:23:13-07:00',
/* author */ (''),
/* organization */ (''),
/* preprocessor_version */ 'ST-DEVELOPER v20.2',
/* originating_system */ 'Autodesk Translation Framework v15.17.0.0',
/* authorisation */ '');

FILE_SCHEMA (('AUTOMOTIVE_DESIGN { 1 0 10303 214 3 1 1 }'));
ENDSEC;

DATA;
#10=MECHANICAL_DESIGN_GEOMETRIC_PRESENTATION_REPRESENTATION('',(#674),#17322);
#570=SHAPE_REPRESENTATION_RELATIONSHIP('SRR','None',#17566,#622);
#622=ADVANCED_BREP_SHAPE_REPRESENTATION('',(#735),#17270);
#674=STYLED_ITEM('',(#17938),#735);
#735=MANIFOLD_SOLID_BREP('Body1',#9052);
#843=FACE_BOUND('',#1990,.T.);
#844=FACE_BOUND('',#1992,.T.);
#1047=PLANE('',#9850);
#1048=PLANE('',#9851);
#1394=FACE_OUTER_BOUND('',#1987,.T.);
#1395=FACE_OUTER_BOUND('',#1988,.T.);
#1396=FACE_OUTER_BOUND('',#1989,.T.);
#1397=FACE_OUTER_BOUND('',#1991,.T.);
#1987=EDGE_LOOP('',(#6422,#6423,#6424,#6425));
#1988=EDGE_LOOP('',(#6426,#6427,#6428,#6429));
#1989=EDGE_LOOP('',(#6430));
#1990=EDGE_LOOP('',(#6431));
#1991=EDGE_LOOP('',(#6432));
#1992=EDGE_LOOP('',(#6433));
#2690=LINE('',#14068,#3301);
#2691=LINE('',#14074,#3302);
#3301=VECTOR('',#11226,0.425);
#3302=VECTOR('',#11233,0.645);
#3914=CIRCLE('',#9845,0.425);
#3915=CIRCLE('',#9846,0.425);
#3916=CIRCLE('',#9848,0.645);
#3917=CIRCLE('',#9849,0.645);
#4377=VERTEX_POINT('',#14065);
#4378=VERTEX_POINT('',#14067);
#4379=VERTEX_POINT('',#14071);
#4380=VERTEX_POINT('',#14073);
#5168=EDGE_CURVE('',#4377,#4377,#3914,.T.);
#5169=EDGE_CURVE('',#4377,#4378,#2690,.T.);
#5170=EDGE_CURVE('',#4378,#4378,#3915,.T.);
#5171=EDGE_CURVE('',#4379,#4379,#3916,.T.);
#5172=EDGE_CURVE('',#4379,#4380,#2691,.T.);
#5173=EDGE_CURVE('',#4380,#4380,#3917,.T.);
#6422=ORIENTED_EDGE('',*,*,#5168,.F.);
#6423=ORIENTED_EDGE('',*,*,#5169,.T.);
#6424=ORIENTED_EDGE('',*,*,#5170,.T.);
#6425=ORIENTED_EDGE('',*,*,#5169,.F.);
#6426=ORIENTED_EDGE('',*,*,#5171,.F.);
#6427=ORIENTED_EDGE('',*,*,#5172,.T.);
#6428=ORIENTED_EDGE('',*,*,#5173,.T.);
#6429=ORIENTED_EDGE('',*,*,#5172,.F.);
#6430=ORIENTED_EDGE('',*,*,#5171,.T.);
#6431=ORIENTED_EDGE('',*,*,#5168,.T.);
#6432=ORIENTED_EDGE('',*,*,#5173,.F.);
#6433=ORIENTED_EDGE('',*,*,#5170,.F.);
#8368=CYLINDRICAL_SURFACE('',#9844,0.425);
#8369=CYLINDRICAL_SURFACE('',#9847,0.645);
#8585=ADVANCED_FACE('',(#1394),#8368,.F.);
#8586=ADVANCED_FACE('',(#1395),#8369,.T.);
#8587=ADVANCED_FACE('',(#1396,#843),#1047,.T.);
#8588=ADVANCED_FACE('',(#1397,#844),#1048,.F.);
#9052=CLOSED_SHELL('',(#8585,#8586,#8587,#8588));
#9843=AXIS2_PLACEMENT_3D('',#14063,#11220,#11221);
#9844=AXIS2_PLACEMENT_3D('',#14064,#11222,#11223);
#9845=AXIS2_PLACEMENT_3D('',#14066,#11224,#11225);
#9846=AXIS2_PLACEMENT_3D('',#14069,#11227,#11228);
#9847=AXIS2_PLACEMENT_3D('',#14070,#11229,#11230);
#9848=AXIS2_PLACEMENT_3D('',#14072,#11231,#11232);
#9849=AXIS2_PLACEMENT_3D('',#14075,#11234,#11235);
#9850=AXIS2_PLACEMENT_3D('',#14076,#11236,#11237);
#9851=AXIS2_PLACEMENT_3D('',#14077,#11238,#11239);
#11220=DIRECTION('axis',(0.,0.,1.));
#11221=DIRECTION('refdir',(1.,0.,0.));
#11222=DIRECTION('center_axis',(0.,0.,1.));
#11223=DIRECTION('ref_axis',(1.,0.,0.));
#11224=DIRECTION('center_axis',(0.,0.,-1.));
#11225=DIRECTION('ref_axis',(1.,0.,0.));
#11226=DIRECTION('',(0.,0.,-1.));
#11227=DIRECTION('center_axis',(0.,0.,-1.));
#11228=DIRECTION('ref_axis',(1.,0.,0.));
#11229=DIRECTION('center_axis',(0.,0.,1.));
#11230=DIRECTION('ref_axis',(1.,0.,0.));
#11231=DIRECTION('center_axis',(0.,0.,1.));
#11232=DIRECTION('ref_axis',(1.,0.,0.));
#11233=DIRECTION('',(0.,0.,-1.));
#11234=DIRECTION('center_axis',(0.,0.,1.));
#11235=DIRECTION('ref_axis',(1.,0.,0.));
#11236=DIRECTION('center_axis',(0.,0.,1.));
#11237=DIRECTION('ref_axis',(1.,0.,0.));
#11238=DIRECTION('center_axis',(0.,0.,1.));
#11239=DIRECTION('ref_axis',(1.,0.,0.));
#14063=CARTESIAN_POINT('',(0.,0.,0.));
#14064=CARTESIAN_POINT('Origin',(4.75,-7.,6.67));
#14065=CARTESIAN_POINT('',(4.325,-7.,7.87));
#14066=CARTESIAN_POINT('Origin',(4.75,-7.,7.87));
#14067=CARTESIAN_POINT('',(4.325,-7.,6.67));
#14068=CARTESIAN_POINT('',(4.325,-7.,6.67));
#14069=CARTESIAN_POINT('Origin',(4.75,-7.,6.67));
#14070=CARTESIAN_POINT('Origin',(4.75,-7.,6.67));
#14071=CARTESIAN_POINT('',(4.105,-7.,7.87));
#14072=CARTESIAN_POINT('Origin',(4.75,-7.,7.87));
#14073=CARTESIAN_POINT('',(4.105,-7.,6.67));
#14074=CARTESIAN_POINT('',(4.105,-7.,6.67));
#14075=CARTESIAN_POINT('Origin',(4.75,-7.,6.67));
#14076=CARTESIAN_POINT('Origin',(4.75,-7.,7.87));
#14077=CARTESIAN_POINT('Origin',(4.75,-7.,6.67));
#17209=UNCERTAINTY_MEASURE_WITH_UNIT(LENGTH_MEASURE(0.001),#17323,
'DISTANCE_ACCURACY_VALUE',
'Maximum model space distance between geometric entities at asserted c
onnectivities');
#17261=UNCERTAINTY_MEASURE_WITH_UNIT(LENGTH_MEASURE(0.001),#17323,
'DISTANCE_ACCURACY_VALUE',
'Maximum model space distance between geometric entities at asserted c
onnectivities');
#17270=(
GEOMETRIC_REPRESENTATION_CONTEXT(3)
GLOBAL_UNCERTAINTY_ASSIGNED_CONTEXT((#17209))
GLOBAL_UNIT_ASSIGNED_CONTEXT((#17323,#17325,#17326))
REPRESENTATION_CONTEXT('','3D')
);
#17322=(
GEOMETRIC_REPRESENTATION_CONTEXT(3)
GLOBAL_UNCERTAINTY_ASSIGNED_CONTEXT((#17261))
GLOBAL_UNIT_ASSIGNED_CONTEXT((#17323,#17325,#17326))
REPRESENTATION_CONTEXT('','3D')
);
#17323=(
LENGTH_UNIT()
NAMED_UNIT(*)
SI_UNIT(.CENTI.,.METRE.)
);
#17325=(
NAMED_UNIT(*)
PLANE_ANGLE_UNIT()
SI_UNIT($,.RADIAN.)
);
#17326=(
NAMED_UNIT(*)
SI_UNIT($,.STERADIAN.)
SOLID_ANGLE_UNIT()
);
#17335=SHAPE_DEFINITION_REPRESENTATION(#17395,#17566);
#17395=PRODUCT_DEFINITION_SHAPE('',$,#17627);
#17566=SHAPE_REPRESENTATION('',(#9843),#17270);
#17618=PRODUCT_DEFINITION_CONTEXT('part definition',#17800,'design');
#17627=PRODUCT_DEFINITION('Bearing bolt reducer (3)',
'Bearing bolt reducer (3)',#17687,#17618);
#17687=PRODUCT_DEFINITION_FORMATION('',$,#17810);
#17800=APPLICATION_CONTEXT(
'Core Data for Automotive Mechanical Design Process');
#17801=PRODUCT_CONTEXT('part definition',#17800,'mechanical');
#17810=PRODUCT('Bearing bolt reducer (3)','Bearing bolt reducer (3)',
'Bearing bolt reducer (3)',(#17801));
#17932=COLOUR_RGB('Black',0.12,0.14,0.17);
#17933=FILL_AREA_STYLE_COLOUR('',#17932);
#17934=FILL_AREA_STYLE('',(#17933));
#17935=SURFACE_STYLE_FILL_AREA(#17934);
#17936=SURFACE_SIDE_STYLE('',(#17935));
#17937=SURFACE_STYLE_USAGE(.BOTH.,#17936);
#17938=PRESENTATION_STYLE_ASSIGNMENT((#17937));
ENDSEC;
END-ISO-10303-21;
